ISO-10303-21;
HEADER;
/* Generated by software containing ST-Developer
 * from STEP Tools, Inc. (www.steptools.com) 
 */

FILE_DESCRIPTION(
/* description */ ('Spring compression tester'),
/* implementation_level */ '2;1');

FILE_NAME(
/* name */ 'M4x30 nut screw.step',
/* time_stamp */ '2026-10-28T03:24:11-07:00',
/* author */ (''),
/* organization */ (''),
/* preprocessor_version */ 'ST-DEVELOPER v20.2',
/* originating_system */ 'Autodesk Translation Framework v15.17.0.0',
/* authorisation */ '');

FILE_SCHEMA (('AUTOMOTIVE_DESIGN { 1 0 10303 214 3 1 1 }'));
ENDSEC;

DATA;
#10=MECHANICAL_DESIGN_GEOMETRIC_PRESENTATION_REPRESENTATION('',(#1167),#43521);
#935=ORIENTED_CLOSED_SHELL('',*,#18608,.F.);
#942=BREP_WITH_VOIDS('Body1',#18609,(#935));
#971=CONICAL_SURFACE('',#20753,0.325,0.785398163397448);
#972=CONICAL_SURFACE('',#20757,0.335,0.785398163397448);
#973=CONICAL_SURFACE('',#20761,0.21,0.463647609000806);
#1032=SHAPE_REPRESENTATION_RELATIONSHIP('SRR','None',#43848,#1092);
#1092=ADVANCED_BREP_SHAPE_REPRESENTATION('',(#942),#43508);
#1167=STYLED_ITEM('',(#44209),#942);
#1562=FACE_BOUND('',#4335,.T.);
#1563=FACE_BOUND('',#4343,.T.);
#2087=PLANE('',#20737);
#2088=PLANE('',#20738);
#2089=PLANE('',#20739);
#2090=PLANE('',#20740);
#2091=PLANE('',#20741);
#2092=PLANE('',#20742);
#2093=PLANE('',#20743);
#2094=PLANE('',#20744);
#2095=PLANE('',#20745);
#2096=PLANE('',#20750);
#2097=PLANE('',#20751);
#2098=PLANE('',#20759);
#2964=FACE_OUTER_BOUND('',#4326,.T.);
#2965=FACE_OUTER_BOUND('',#4327,.T.);
#2966=FACE_OUTER_BOUND('',#4328,.T.);
#2967=FACE_OUTER_BOUND('',#4329,.T.);
#2968=FACE_OUTER_BOUND('',#4330,.T.);
#2969=FACE_OUTER_BOUND('',#4331,.T.);
#2970=FACE_OUTER_BOUND('',#4332,.T.);
#2971=FACE_OUTER_BOUND('',#4333,.T.);
#2972=FACE_OUTER_BOUND('',#4334,.T.);
#2973=FACE_OUTER_BOUND('',#4336,.T.);
#2974=FACE_OUTER_BOUND('',#4337,.T.);
#2975=FACE_OUTER_BOUND('',#4338,.T.);
#2976=FACE_OUTER_BOUND('',#4339,.T.);
#2977=FACE_OUTER_BOUND('',#4340,.T.);
#2978=FACE_OUTER_BOUND('',#4341,.T.);
#2979=FACE_OUTER_BOUND('',#4342,.T.);
#2980=FACE_OUTER_BOUND('',#4344,.T.);
#2981=FACE_OUTER_BOUND('',#4345,.T.);
#4326=EDGE_LOOP('',(#15843,#15844,#15845,#15846));
#4327=EDGE_LOOP('',(#15847,#15848,#15849,#15850));
#4328=EDGE_LOOP('',(#15851,#15852,#15853,#15854));
#4329=EDGE_LOOP('',(#15855,#15856,#15857,#15858));
#4330=EDGE_LOOP('',(#15859,#15860,#15861,#15862));
#4331=EDGE_LOOP('',(#15863,#15864,#15865,#15866));
#4332=EDGE_LOOP('',(#15867,#15868,#15869,#15870,#15871,#15872));
#4333=EDGE_LOOP('',(#15873,#15874,#15875,#15876,#15877,#15878));
#4334=EDGE_LOOP('',(#15879));
#4335=EDGE_LOOP('',(#15880));
#4336=EDGE_LOOP('',(#15881,#15882,#15883,#15884));
#4337=EDGE_LOOP('',(#15885));
#4338=EDGE_LOOP('',(#15886));
#4339=EDGE_LOOP('',(#15887,#15888,#15889,#15890));
#4340=EDGE_LOOP('',(#15891,#15892,#15893,#15894));
#4341=EDGE_LOOP('',(#15895,#15896,#15897,#15898));
#4342=EDGE_LOOP('',(#15899));
#4343=EDGE_LOOP('',(#15900));
#4344=EDGE_LOOP('',(#15901,#15902,#15903,#15904));
#4345=EDGE_LOOP('',(#15905,#15906,#15907,#15908));
#5750=LINE('',#33010,#7182);
#5751=LINE('',#33012,#7183);
#5752=LINE('',#33014,#7184);
#5753=LINE('',#33015,#7185);
#5754=LINE('',#33018,#7186);
#5755=LINE('',#33020,#7187);
#5756=LINE('',#33021,#7188);
#5757=LINE('',#33024,#7189);
#5758=LINE('',#33026,#7190);
#5759=LINE('',#33027,#7191);
#5760=LINE('',#33030,#7192);
#5761=LINE('',#33032,#7193);
#5762=LINE('',#33033,#7194);
#5763=LINE('',#33036,#7195);
#5764=LINE('',#33038,#7196);
#5765=LINE('',#33039,#7197);
#5766=LINE('',#33041,#7198);
#5767=LINE('',#33042,#7199);
#5768=LINE('',#33052,#7200);
#5769=LINE('',#33061,#7201);
#5770=LINE('',#33065,#7202);
#5771=LINE('',#33069,#7203);
#5772=LINE('',#33076,#7204);
#5773=LINE('',#33078,#7205);
#7182=VECTOR('',#25248,1.);
#7183=VECTOR('',#25249,1.);
#7184=VECTOR('',#25250,1.);
#7185=VECTOR('',#25251,1.);
#7186=VECTOR('',#25254,1.);
#7187=VECTOR('',#25255,1.);
#7188=VECTOR('',#25256,1.);
#7189=VECTOR('',#25259,1.);
#7190=VECTOR('',#25260,1.);
#7191=VECTOR('',#25261,1.);
#7192=VECTOR('',#25264,1.);
#7193=VECTOR('',#25265,1.);
#7194=VECTOR('',#25266,1.);
#7195=VECTOR('',#25269,1.);
#7196=VECTOR('',#25270,1.);
#7197=VECTOR('',#25271,1.);
#7198=VECTOR('',#25274,1.);
#7199=VECTOR('',#25275,1.);
#7200=VECTOR('',#25288,0.2);
#7201=VECTOR('',#25301,0.325);
#7202=VECTOR('',#25306,0.35);
#7203=VECTOR('',#25311,0.335);
#7204=VECTOR('',#25320,0.21);
#7205=VECTOR('',#25323,0.2);
#8062=CIRCLE('',#20746,0.2);
#8063=CIRCLE('',#20747,0.1954);
#8064=CIRCLE('',#20749,0.2);
#8065=CIRCLE('',#20752,0.3);
#8066=CIRCLE('',#20754,0.35);
#8067=CIRCLE('',#20756,0.35);
#8068=CIRCLE('',#20758,0.32);
#8069=CIRCLE('',#20760,0.22);
#8070=CIRCLE('',#20762,0.1954);
#9356=VERTEX_POINT('',#33008);
#9357=VERTEX_POINT('',#33009);
#9358=VERTEX_POINT('',#33011);
#9359=VERTEX_POINT('',#33013);
#9360=VERTEX_POINT('',#33017);
#9361=VERTEX_POINT('',#33019);
#9362=VERTEX_POINT('',#33023);
#9363=VERTEX_POINT('',#33025);
#9364=VERTEX_POINT('',#33029);
#9365=VERTEX_POINT('',#33031);
#9366=VERTEX_POINT('',#33035);
#9367=VERTEX_POINT('',#33037);
#9368=VERTEX_POINT('',#33046);
#9369=VERTEX_POINT('',#33048);
#9370=VERTEX_POINT('',#33051);
#9371=VERTEX_POINT('',#33056);
#9372=VERTEX_POINT('',#33059);
#9373=VERTEX_POINT('',#33063);
#9374=VERTEX_POINT('',#33067);
#9375=VERTEX_POINT('',#33071);
#9376=VERTEX_POINT('',#33074);
#11586=EDGE_CURVE('',#9356,#9357,#5750,.T.);
#11587=EDGE_CURVE('',#9357,#9358,#5751,.T.);
#11588=EDGE_CURVE('',#9358,#9359,#5752,.T.);
#11589=EDGE_CURVE('',#9356,#9359,#5753,.T.);
#11590=EDGE_CURVE('',#9357,#9360,#5754,.T.);
#11591=EDGE_CURVE('',#9360,#9361,#5755,.T.);
#11592=EDGE_CURVE('',#9361,#9358,#5756,.T.);
#11593=EDGE_CURVE('',#9360,#9362,#5757,.T.);
#11594=EDGE_CURVE('',#9362,#9363,#5758,.T.);
#11595=EDGE_CURVE('',#9363,#9361,#5759,.T.);
#11596=EDGE_CURVE('',#9362,#9364,#5760,.T.);
#11597=EDGE_CURVE('',#9364,#9365,#5761,.T.);
#11598=EDGE_CURVE('',#9365,#9363,#5762,.T.);
#11599=EDGE_CURVE('',#9364,#9366,#5763,.T.);
#11600=EDGE_CURVE('',#9366,#9367,#5764,.T.);
#11601=EDGE_CURVE('',#9367,#9365,#5765,.T.);
#11602=EDGE_CURVE('',#9366,#9356,#5766,.T.);
#11603=EDGE_CURVE('',#9359,#9367,#5767,.T.);
#11604=EDGE_CURVE('',#9368,#9368,#8062,.T.);
#11605=EDGE_CURVE('',#9369,#9369,#8063,.T.);
#11606=EDGE_CURVE('',#9368,#9370,#5768,.T.);
#11607=EDGE_CURVE('',#9370,#9370,#8064,.T.);
#11608=EDGE_CURVE('',#9371,#9371,#8065,.T.);
#11609=EDGE_CURVE('',#9372,#9372,#8066,.T.);
#11610=EDGE_CURVE('',#9372,#9371,#5769,.T.);
#11611=EDGE_CURVE('',#9373,#9373,#8067,.T.);
#11612=EDGE_CURVE('',#9373,#9372,#5770,.T.);
#11613=EDGE_CURVE('',#9374,#9374,#8068,.T.);
#11614=EDGE_CURVE('',#9374,#9373,#5771,.T.);
#11615=EDGE_CURVE('',#9375,#9375,#8069,.T.);
#11616=EDGE_CURVE('',#9376,#9376,#8070,.F.);
#11617=EDGE_CURVE('',#9376,#9375,#5772,.T.);
#11618=EDGE_CURVE('',#9369,#9376,#5773,.T.);
#15843=ORIENTED_EDGE('',*,*,#11586,.T.);
#15844=ORIENTED_EDGE('',*,*,#11587,.T.);
#15845=ORIENTED_EDGE('',*,*,#11588,.T.);
#15846=ORIENTED_EDGE('',*,*,#11589,.F.);
#15847=ORIENTED_EDGE('',*,*,#11590,.T.);
#15848=ORIENTED_EDGE('',*,*,#11591,.T.);
#15849=ORIENTED_EDGE('',*,*,#11592,.T.);
#15850=ORIENTED_EDGE('',*,*,#11587,.F.);
#15851=ORIENTED_EDGE('',*,*,#11593,.T.);
#15852=ORIENTED_EDGE('',*,*,#11594,.T.);
#15853=ORIENTED_EDGE('',*,*,#11595,.T.);
#15854=ORIENTED_EDGE('',*,*,#11591,.F.);
#15855=ORIENTED_EDGE('',*,*,#11596,.T.);
#15856=ORIENTED_EDGE('',*,*,#11597,.T.);
#15857=ORIENTED_EDGE('',*,*,#11598,.T.);
#15858=ORIENTED_EDGE('',*,*,#11594,.F.);
#15859=ORIENTED_EDGE('',*,*,#11599,.T.);
#15860=ORIENTED_EDGE('',*,*,#11600,.T.);
#15861=ORIENTED_EDGE('',*,*,#11601,.T.);
#15862=ORIENTED_EDGE('',*,*,#11597,.F.);
#15863=ORIENTED_EDGE('',*,*,#11602,.T.);
#15864=ORIENTED_EDGE('',*,*,#11589,.T.);
#15865=ORIENTED_EDGE('',*,*,#11603,.T.);
#15866=ORIENTED_EDGE('',*,*,#11600,.F.);
#15867=ORIENTED_EDGE('',*,*,#11602,.F.);
#15868=ORIENTED_EDGE('',*,*,#11599,.F.);
#15869=ORIENTED_EDGE('',*,*,#11596,.F.);
#15870=ORIENTED_EDGE('',*,*,#11593,.F.);
#15871=ORIENTED_EDGE('',*,*,#11590,.F.);
#15872=ORIENTED_EDGE('',*,*,#11586,.F.);
#15873=ORIENTED_EDGE('',*,*,#11603,.F.);
#15874=ORIENTED_EDGE('',*,*,#11588,.F.);
#15875=ORIENTED_EDGE('',*,*,#11592,.F.);
#15876=ORIENTED_EDGE('',*,*,#11595,.F.);
#15877=ORIENTED_EDGE('',*,*,#11598,.F.);
#15878=ORIENTED_EDGE('',*,*,#11601,.F.);
#15879=ORIENTED_EDGE('',*,*,#11604,.T.);
#15880=ORIENTED_EDGE('',*,*,#11605,.F.);
#15881=ORIENTED_EDGE('',*,*,#11604,.F.);
#15882=ORIENTED_EDGE('',*,*,#11606,.T.);
#15883=ORIENTED_EDGE('',*,*,#11607,.T.);
#15884=ORIENTED_EDGE('',*,*,#11606,.F.);
#15885=ORIENTED_EDGE('',*,*,#11607,.F.);
#15886=ORIENTED_EDGE('',*,*,#11608,.F.);
#15887=ORIENTED_EDGE('',*,*,#11609,.F.);
#15888=ORIENTED_EDGE('',*,*,#11610,.T.);
#15889=ORIENTED_EDGE('',*,*,#11608,.T.);
#15890=ORIENTED_EDGE('',*,*,#11610,.F.);
#15891=ORIENTED_EDGE('',*,*,#11611,.F.);
#15892=ORIENTED_EDGE('',*,*,#11612,.T.);
#15893=ORIENTED_EDGE('',*,*,#11609,.T.);
#15894=ORIENTED_EDGE('',*,*,#11612,.F.);
#15895=ORIENTED_EDGE('',*,*,#11613,.F.);
#15896=ORIENTED_EDGE('',*,*,#11614,.T.);
#15897=ORIENTED_EDGE('',*,*,#11611,.T.);
#15898=ORIENTED_EDGE('',*,*,#11614,.F.);
#15899=ORIENTED_EDGE('',*,*,#11613,.T.);
#15900=ORIENTED_EDGE('',*,*,#11615,.F.);
#15901=ORIENTED_EDGE('',*,*,#11616,.F.);
#15902=ORIENTED_EDGE('',*,*,#11617,.T.);
#15903=ORIENTED_EDGE('',*,*,#11615,.T.);
#15904=ORIENTED_EDGE('',*,*,#11617,.F.);
#15905=ORIENTED_EDGE('',*,*,#11605,.T.);
#15906=ORIENTED_EDGE('',*,*,#11618,.T.);
#15907=ORIENTED_EDGE('',*,*,#11616,.T.);
#15908=ORIENTED_EDGE('',*,*,#11618,.F.);
#17339=CYLINDRICAL_SURFACE('',#20748,0.2);
#17340=CYLINDRICAL_SURFACE('',#20755,0.35);
#17341=CYLINDRICAL_SURFACE('',#20763,0.1954);
#18288=ADVANCED_FACE('',(#2964),#2087,.F.);
#18289=ADVANCED_FACE('',(#2965),#2088,.F.);
#18290=ADVANCED_FACE('',(#2966),#2089,.F.);
#18291=ADVANCED_FACE('',(#2967),#2090,.F.);
#18292=ADVANCED_FACE('',(#2968),#2091,.F.);
#18293=ADVANCED_FACE('',(#2969),#2092,.F.);
#18294=ADVANCED_FACE('',(#2970),#2093,.F.);
#18295=ADVANCED_FACE('',(#2971),#2094,.F.);
#18296=ADVANCED_FACE('',(#2972,#1562),#2095,.T.);
#18297=ADVANCED_FACE('',(#2973),#17339,.T.);
#18298=ADVANCED_FACE('',(#2974),#2096,.F.);
#18299=ADVANCED_FACE('',(#2975),#2097,.T.);
#18300=ADVANCED_FACE('',(#2976),#971,.T.);
#18301=ADVANCED_FACE('',(#2977),#17340,.T.);
#18302=ADVANCED_FACE('',(#2978),#972,.T.);
#18303=ADVANCED_FACE('',(#2979,#1563),#2098,.T.);
#18304=ADVANCED_FACE('',(#2980),#973,.T.);
#18305=ADVANCED_FACE('',(#2981),#17341,.T.);
#18608=CLOSED_SHELL('',(#18288,#18289,#18290,#18291,#18292,#18293,#18294,
#18295));
#18609=CLOSED_SHELL('',(#18296,#18297,#18298,#18299,#18300,#18301,#18302,
#18303,#18304,#18305));
#20736=AXIS2_PLACEMENT_3D('',#33006,#25244,#25245);
#20737=AXIS2_PLACEMENT_3D('',#33007,#25246,#25247);
#20738=AXIS2_PLACEMENT_3D('',#33016,#25252,#25253);
#20739=AXIS2_PLACEMENT_3D('',#33022,#25257,#25258);
#20740=AXIS2_PLACEMENT_3D('',#33028,#25262,#25263);
#20741=AXIS2_PLACEMENT_3D('',#33034,#25267,#25268);
#20742=AXIS2_PLACEMENT_3D('',#33040,#25272,#25273);
#20743=AXIS2_PLACEMENT_3D('',#33043,#25276,#25277);
#20744=AXIS2_PLACEMENT_3D('',#33044,#25278,#25279);
#20745=AXIS2_PLACEMENT_3D('',#33045,#25280,#25281);
#20746=AXIS2_PLACEMENT_3D('',#33047,#25282,#25283);
#20747=AXIS2_PLACEMENT_3D('',#33049,#25284,#25285);
#20748=AXIS2_PLACEMENT_3D('',#33050,#25286,#25287);
#20749=AXIS2_PLACEMENT_3D('',#33053,#25289,#25290);
#20750=AXIS2_PLACEMENT_3D('',#33054,#25291,#25292);
#20751=AXIS2_PLACEMENT_3D('',#33055,#25293,#25294);
#20752=AXIS2_PLACEMENT_3D('',#33057,#25295,#25296);
#20753=AXIS2_PLACEMENT_3D('',#33058,#25297,#25298);
#20754=AXIS2_PLACEMENT_3D('',#33060,#25299,#25300);
#20755=AXIS2_PLACEMENT_3D('',#33062,#25302,#25303);
#20756=AXIS2_PLACEMENT_3D('',#33064,#25304,#25305);
#20757=AXIS2_PLACEMENT_3D('',#33066,#25307,#25308);
#20758=AXIS2_PLACEMENT_3D('',#33068,#25309,#25310);
#20759=AXIS2_PLACEMENT_3D('',#33070,#25312,#25313);
#20760=AXIS2_PLACEMENT_3D('',#33072,#25314,#25315);
#20761=AXIS2_PLACEMENT_3D('',#33073,#25316,#25317);
#20762=AXIS2_PLACEMENT_3D('',#33075,#25318,#25319);
#20763=AXIS2_PLACEMENT_3D('',#33077,#25321,#25322);
#25244=DIRECTION('axis',(0.,0.,1.));
#25245=DIRECTION('refdir',(1.,0.,0.));
#25246=DIRECTION('center_axis',(0.866025403784439,0.,-0.5));
#25247=DIRECTION('ref_axis',(0.5,0.,0.866025403784439));
#25248=DIRECTION('',(-0.5,0.,-0.866025403784439));
#25249=DIRECTION('',(0.,-1.,0.));
#25250=DIRECTION('',(0.5,0.,0.866025403784439));
#25251=DIRECTION('',(0.,-1.,0.));
#25252=DIRECTION('center_axis',(1.60246890531964E-16,0.,-1.));
#25253=DIRECTION('ref_axis',(1.,0.,1.60246890531964E-16));
#25254=DIRECTION('',(-1.,0.,-1.60246890531964E-16));
#25255=DIRECTION('',(0.,-1.,0.));
#25256=DIRECTION('',(1.,0.,1.60246890531964E-16));
#25257=DIRECTION('center_axis',(-0.866025403784439,0.,-0.5));
#25258=DIRECTION('ref_axis',(0.5,0.,-0.866025403784439));
#25259=DIRECTION('',(-0.5,0.,0.866025403784439));
#25260=DIRECTION('',(0.,-1.,0.));
#25261=DIRECTION('',(0.5,0.,-0.866025403784439));
#25262=DIRECTION('center_axis',(-0.866025403784439,0.,0.5));
#25263=DIRECTION('ref_axis',(-0.5,0.,-0.866025403784439));
#25264=DIRECTION('',(0.5,0.,0.866025403784439));
#25265=DIRECTION('',(0.,-1.,0.));
#25266=DIRECTION('',(-0.5,0.,-0.866025403784439));
#25267=DIRECTION('center_axis',(-1.60246890531964E-16,0.,1.));
#25268=DIRECTION('ref_axis',(-1.,0.,-1.60246890531964E-16));
#25269=DIRECTION('',(1.,0.,1.60246890531964E-16));
#25270=DIRECTION('',(0.,-1.,0.));
#25271=DIRECTION('',(-1.,0.,-1.60246890531964E-16));
#25272=DIRECTION('center_axis',(0.866025403784439,0.,0.5));
#25273=DIRECTION('ref_axis',(-0.5,0.,0.866025403784439));
#25274=DIRECTION('',(0.5,0.,-0.866025403784439));
#25275=DIRECTION('',(-0.5,0.,0.866025403784439));
#25276=DIRECTION('center_axis',(0.,1.,0.));
#25277=DIRECTION('ref_axis',(1.,0.,0.));
#25278=DIRECTION('center_axis',(0.,-1.,0.));
#25279=DIRECTION('ref_axis',(0.,0.,-1.));
#25280=DIRECTION('center_axis',(0.,1.,0.));
#25281=DIRECTION('ref_axis',(1.,0.,0.));
#25282=DIRECTION('center_axis',(0.,1.,0.));
#25283=DIRECTION('ref_axis',(1.,0.,0.));
#25284=DIRECTION('center_axis',(0.,1.,0.));
#25285=DIRECTION('ref_axis',(1.,0.,0.));
#25286=DIRECTION('center_axis',(0.,1.,0.));
#25287=DIRECTION('ref_axis',(1.,0.,0.));
#25288=DIRECTION('',(0.,-1.,0.));
#25289=DIRECTION('center_axis',(0.,1.,0.));
#25290=DIRECTION('ref_axis',(1.,0.,0.));
#25291=DIRECTION('center_axis',(0.,1.,0.));
#25292=DIRECTION('ref_axis',(1.,0.,0.));
#25293=DIRECTION('center_axis',(0.,1.,0.));
#25294=DIRECTION('ref_axis',(0.,0.,1.));
#25295=DIRECTION('center_axis',(0.,-1.,0.));
#25296=DIRECTION('ref_axis',(1.,0.,0.));
#25297=DIRECTION('center_axis',(0.,-1.,0.));
#25298=DIRECTION('ref_axis',(1.,0.,0.));
#25299=DIRECTION('center_axis',(0.,-1.,0.));
#25300=DIRECTION('ref_axis',(1.,0.,0.));
#25301=DIRECTION('',(0.707106781186547,0.707106781186548,8.65956056235493E-17));
#25302=DIRECTION('center_axis',(0.,-1.,0.));
#25303=DIRECTION('ref_axis',(1.,0.,0.));
#25304=DIRECTION('center_axis',(0.,-1.,0.));
#25305=DIRECTION('ref_axis',(1.,0.,0.));
#25306=DIRECTION('',(0.,1.,0.));
#25307=DIRECTION('center_axis',(0.,1.,0.));
#25308=DIRECTION('ref_axis',(1.,0.,0.));
#25309=DIRECTION('center_axis',(0.,-1.,0.));
#25310=DIRECTION('ref_axis',(1.,0.,0.));
#25311=DIRECTION('',(-0.707106781186547,0.707106781186548,-8.65956056235493E-17));
#25312=DIRECTION('center_axis',(0.,-1.,0.));
#25313=DIRECTION('ref_axis',(0.,0.,-1.));
#25314=DIRECTION('center_axis',(0.,-1.,0.));
#25315=DIRECTION('ref_axis',(1.,0.,0.));
#25316=DIRECTION('center_axis',(0.,1.,0.));
#25317=DIRECTION('ref_axis',(1.,0.,0.));
#25318=DIRECTION('center_axis',(0.,1.,0.));
#25319=DIRECTION('ref_axis',(1.,0.,0.));
#25320=DIRECTION('',(-0.447213595499958,0.894427190999916,-5.47678698264203E-17));
#25321=DIRECTION('center_axis',(0.,-1.,0.));
#25322=DIRECTION('ref_axis',(1.,0.,0.));
#25323=DIRECTION('',(0.,1.,0.));
#33006=CARTESIAN_POINT('',(0.,0.,0.));
#33007=CARTESIAN_POINT('Origin',(0.0866025403784439,-0.4,-0.15));
#33008=CARTESIAN_POINT('',(0.173205080756888,-0.4,0.));
#33009=CARTESIAN_POINT('',(0.0866025403784439,-0.4,-0.15));
#33010=CARTESIAN_POINT('',(0.173205080756888,-0.4,0.));
#33011=CARTESIAN_POINT('',(0.0866025403784439,-0.64,-0.15));
#33012=CARTESIAN_POINT('',(0.0866025403784439,-0.4,-0.15));
#33013=CARTESIAN_POINT('',(0.173205080756888,-0.64,0.));
#33014=CARTESIAN_POINT('',(0.173205080756888,-0.64,0.));
#33015=CARTESIAN_POINT('',(0.173205080756888,-0.4,0.));
#33016=CARTESIAN_POINT('Origin',(-0.0866025403784438,-0.4,-0.15));
#33017=CARTESIAN_POINT('',(-0.0866025403784438,-0.4,-0.15));
#33018=CARTESIAN_POINT('',(0.0866025403784439,-0.4,-0.15));
#33019=CARTESIAN_POINT('',(-0.0866025403784438,-0.64,-0.15));
#33020=CARTESIAN_POINT('',(-0.0866025403784438,-0.4,-0.15));
#33021=CARTESIAN_POINT('',(0.0866025403784439,-0.64,-0.15));
#33022=CARTESIAN_POINT('Origin',(-0.173205080756888,-0.4,-2.77555756156289E-17));
#33023=CARTESIAN_POINT('',(-0.173205080756888,-0.4,-2.12115047744981E-17));
#33024=CARTESIAN_POINT('',(-0.0866025403784438,-0.4,-0.15));
#33025=CARTESIAN_POINT('',(-0.173205080756888,-0.64,-2.77555756156289E-17));
#33026=CARTESIAN_POINT('',(-0.173205080756888,-0.4,-2.12115047744981E-17));
#33027=CARTESIAN_POINT('',(-0.0866025403784438,-0.64,-0.15));
#33028=CARTESIAN_POINT('Origin',(-0.0866025403784439,-0.4,0.15));
#33029=CARTESIAN_POINT('',(-0.0866025403784439,-0.4,0.15));
#33030=CARTESIAN_POINT('',(-0.173205080756888,-0.4,-2.12115047744981E-17));
#33031=CARTESIAN_POINT('',(-0.0866025403784439,-0.64,0.15));
#33032=CARTESIAN_POINT('',(-0.0866025403784439,-0.4,0.15));
#33033=CARTESIAN_POINT('',(-0.173205080756888,-0.64,-2.12115047744981E-17));
#33034=CARTESIAN_POINT('Origin',(0.0866025403784439,-0.4,0.15));
#33035=CARTESIAN_POINT('',(0.0866025403784439,-0.4,0.15));
#33036=CARTESIAN_POINT('',(-0.0866025403784439,-0.4,0.15));
#33037=CARTESIAN_POINT('',(0.0866025403784439,-0.64,0.15));
#33038=CARTESIAN_POINT('',(0.0866025403784439,-0.4,0.15));
#33039=CARTESIAN_POINT('',(-0.0866025403784439,-0.64,0.15));
#33040=CARTESIAN_POINT('Origin',(0.173205080756888,-0.4,0.));
#33041=CARTESIAN_POINT('',(0.0866025403784439,-0.4,0.15));
#33042=CARTESIAN_POINT('',(0.0866025403784439,-0.64,0.15));
#33043=CARTESIAN_POINT('Origin',(0.,-0.4,-2.77555756156289E-17));
#33044=CARTESIAN_POINT('Origin',(0.,-0.64,-2.77555756156289E-17));
#33045=CARTESIAN_POINT('Origin',(0.,-1.5,0.));
#33046=CARTESIAN_POINT('',(-0.2,-1.5,2.44929359829471E-17));
#33047=CARTESIAN_POINT('Origin',(0.,-1.5,0.));
#33048=CARTESIAN_POINT('',(-0.1954,-1.5,2.39295984553393E-17));
#33049=CARTESIAN_POINT('Origin',(0.,-1.5,0.));
#33050=CARTESIAN_POINT('Origin',(0.,-3.,0.));
#33051=CARTESIAN_POINT('',(-0.2,-3.,2.44929359829471E-17));
#33052=CARTESIAN_POINT('',(-0.2,-3.,2.44929359829471E-17));
#33053=CARTESIAN_POINT('Origin',(0.,-3.,0.));
#33054=CARTESIAN_POINT('Origin',(0.,-3.,0.));
#33055=CARTESIAN_POINT('Origin',(0.3,0.4,0.));
#33056=CARTESIAN_POINT('',(-0.3,0.4,-3.67394039744206E-17));
#33057=CARTESIAN_POINT('Origin',(0.,0.4,0.));
#33058=CARTESIAN_POINT('Origin',(0.,0.375,0.));
#33059=CARTESIAN_POINT('',(-0.35,0.35,-4.28626379701573E-17));
#33060=CARTESIAN_POINT('Origin',(0.,0.35,0.));
#33061=CARTESIAN_POINT('',(-0.325,0.375,-3.9801020972289E-17));
#33062=CARTESIAN_POINT('Origin',(0.,0.19,0.));
#33063=CARTESIAN_POINT('',(-0.35,0.03,-4.28626379701574E-17));
#33064=CARTESIAN_POINT('Origin',(0.,0.03,0.));
#33065=CARTESIAN_POINT('',(-0.35,0.19,-4.28626379701574E-17));
#33066=CARTESIAN_POINT('Origin',(0.,0.0149999999999999,0.));
#33067=CARTESIAN_POINT('',(-0.32,-3.29597460435593E-17,-3.91886975727153E-17));
#33068=CARTESIAN_POINT('Origin',(0.,0.,0.));
#33069=CARTESIAN_POINT('',(-0.335,0.0149999999999999,-4.10256677714363E-17));
#33070=CARTESIAN_POINT('Origin',(0.22,0.,0.));
#33071=CARTESIAN_POINT('',(-0.22,-6.93889390390723E-18,-2.69422295812418E-17));
#33072=CARTESIAN_POINT('Origin',(0.,0.,0.));
#33073=CARTESIAN_POINT('Origin',(0.,-0.02,0.));
#33074=CARTESIAN_POINT('',(-0.1954,-0.0492,2.39295984553393E-17));
#33075=CARTESIAN_POINT('Origin',(0.,-0.0492,0.));
#33076=CARTESIAN_POINT('',(-0.21,-0.02,-2.57175827820944E-17));
#33077=CARTESIAN_POINT('Origin',(0.,-0.8,0.));
#33078=CARTESIAN_POINT('',(-0.1954,-0.8,-2.39295984553393E-17));
#43440=UNCERTAINTY_MEASURE_WITH_UNIT(LENGTH_MEASURE(0.001),#43522,
'DISTANCE_ACCURACY_VALUE',
'Maximum model space distance between geometric entities at asserted c
onnectivities');
#43453=UNCERTAINTY_MEASURE_WITH_UNIT(LENGTH_MEASURE(0.001),#43522,
'DISTANCE_ACCURACY_VALUE',
'Maximum model space distance between geometric entities at asserted c
onnectivities');
#43508=(
GEOMETRIC_REPRESENTATION_CONTEXT(3)
GLOBAL_UNCERTAINTY_ASSIGNED_CONTEXT((#43440))
GLOBAL_UNIT_ASSIGNED_CONTEXT((#43522,#43524,#43525))
REPRESENTATION_CONTEXT('','3D')
);
#43521=(
GEOMETRIC_REPRESENTATION_CONTEXT(3)
GLOBAL_UNCERTAINTY_ASSIGNED_CONTEXT((#43453))
GLOBAL_UNIT_ASSIGNED_CONTEXT((#43522,#43524,#43525))
REPRESENTATION_CONTEXT('','3D')
);
#43522=(
LENGTH_UNIT()
NAMED_UNIT(*)
SI_UNIT(.CENTI.,.METRE.)
);
#43524=(
NAMED_UNIT(*)
PLANE_ANGLE_UNIT()
SI_UNIT($,.RADIAN.)
);
#43525=(
NAMED_UNIT(*)
SI_UNIT($,.STERADIAN.)
SOLID_ANGLE_UNIT()
);
#43580=SHAPE_DEFINITION_REPRESENTATION(#43659,#43848);
#43659=PRODUCT_DEFINITION_SHAPE('',$,#43916);
#43848=SHAPE_REPRESENTATION('',(#20736),#43508);
#43861=PRODUCT_DEFINITION_CONTEXT('part definition',#44064,'design');
#43916=PRODUCT_DEFINITION('M4x30 nut screw','M4x30 nut screw',#43983,#43861);
#43983=PRODUCT_DEFINITION_FORMATION('',$,#44120);
#44064=APPLICATION_CONTEXT(
'Core Data for Automotive Mechanical Design Process');
#44065=PRODUCT_CONTEXT('part definition',#44064,'mechanical');
#44120=PRODUCT('M4x30 nut screw','M4x30 nut screw','M4x30 nut screw',(#44065));
#44203=COLOUR_RGB('Black',0.12,0.14,0.17);
#44204=FILL_AREA_STYLE_COLOUR('',#44203);
#44205=FILL_AREA_STYLE('',(#44204));
#44206=SURFACE_STYLE_FILL_AREA(#44205);
#44207=SURFACE_SIDE_STYLE('',(#44206));
#44208=SURFACE_STYLE_USAGE(.BOTH.,#44207);
#44209=PRESENTATION_STYLE_ASSIGNMENT((#44208));
ENDSEC;
END-ISO-10303-21;
